ISO-10303-21;
HEADER;
/* Generated by software containing ST-Developer
 * from STEP Tools, Inc. (www.steptools.com) 
 */

FILE_DESCRIPTION(
/* description */ (''),
/* implementation_level */ '2;1');

FILE_NAME(
/* name */ '08_Shaft_Lip_Seal_5-8x1-1-8.step',
/* time_stamp */ '2026-10-26T06:59:52-07:00',
/* author */ (''),
/* organization */ (''),
/* preprocessor_version */ 'ST-DEVELOPER v20.2',
/* originating_system */ 'Autodesk Translation Framework v15.15.0.0',
/* authorisation */ '');

FILE_SCHEMA (('AUTOMOTIVE_DESIGN { 1 0 10303 214 3 1 1 }'));
ENDSEC;

DATA;
#10=MECHANICAL_DESIGN_GEOMETRIC_PRESENTATION_REPRESENTATION('',(#170),#46395);
#142=SHAPE_REPRESENTATION_RELATIONSHIP('SRR','None',#46462,#156);
#156=ADVANCED_BREP_SHAPE_REPRESENTATION('',(#184),#46387);
#170=STYLED_ITEM('',(#46603),#184);
#184=MANIFOLD_SOLID_BREP('Body1',#24943);
#523=CYLINDRICAL_SURFACE('',#26444,7.94);
#524=CYLINDRICAL_SURFACE('',#26448,14.29);
#525=CYLINDRICAL_SURFACE('',#26452,12.);
#657=FACE_BOUND('',#4164,.T.);
#658=FACE_BOUND('',#4168,.T.);
#659=FACE_BOUND('',#4171,.T.);
#660=FACE_BOUND('',#4174,.T.);
#1512=PLANE('',#26440);
#1513=PLANE('',#26446);
#1514=PLANE('',#26450);
#1515=PLANE('',#26454);
#2760=FACE_OUTER_BOUND('',#4162,.T.);
#2761=FACE_OUTER_BOUND('',#4163,.T.);
#2762=FACE_OUTER_BOUND('',#4165,.T.);
#2763=FACE_OUTER_BOUND('',#4166,.T.);
#2764=FACE_OUTER_BOUND('',#4167,.T.);
#2765=FACE_OUTER_BOUND('',#4169,.T.);
#2766=FACE_OUTER_BOUND('',#4170,.T.);
#2767=FACE_OUTER_BOUND('',#4172,.T.);
#2768=FACE_OUTER_BOUND('',#4173,.T.);
#2769=FACE_OUTER_BOUND('',#4175,.T.);
#4162=EDGE_LOOP('',(#22088,#22089,#22090,#22091,#22092));
#4163=EDGE_LOOP('',(#22093));
#4164=EDGE_LOOP('',(#22094));
#4165=EDGE_LOOP('',(#22095,#22096,#22097,#22098,#22099));
#4166=EDGE_LOOP('',(#22100,#22101,#22102,#22103));
#4167=EDGE_LOOP('',(#22104));
#4168=EDGE_LOOP('',(#22105));
#4169=EDGE_LOOP('',(#22106,#22107,#22108,#22109));
#4170=EDGE_LOOP('',(#22110));
#4171=EDGE_LOOP('',(#22111));
#4172=EDGE_LOOP('',(#22112,#22113,#22114,#22115));
#4173=EDGE_LOOP('',(#22116));
#4174=EDGE_LOOP('',(#22117));
#4175=EDGE_LOOP('',(#22118,#22119,#22120,#22121));
#6927=LINE('',#40213,#9796);
#6928=LINE('',#40221,#9797);
#6929=LINE('',#40225,#9798);
#6930=LINE('',#40232,#9799);
#6931=LINE('',#40238,#9800);
#6932=LINE('',#40244,#9801);
#9796=VECTOR('',#31992,9.47407799863808);
#9797=VECTOR('',#32003,10.15);
#9798=VECTOR('',#32008,7.94);
#9799=VECTOR('',#32017,14.29);
#9800=VECTOR('',#32024,12.);
#9801=VECTOR('',#32033,9.07);
#10589=CIRCLE('',#26437,9.69815599727615);
#10590=CIRCLE('',#26438,9.69815599727615);
#10591=CIRCLE('',#26439,9.25);
#10592=CIRCLE('',#26441,7.94);
#10593=CIRCLE('',#26443,10.8);
#10594=CIRCLE('',#26445,7.94);
#10595=CIRCLE('',#26447,14.29);
#10596=CIRCLE('',#26449,14.29);
#10597=CIRCLE('',#26451,12.);
#10598=CIRCLE('',#26453,12.);
#10599=CIRCLE('',#26455,10.2);
#12544=VERTEX_POINT('',#40208);
#12545=VERTEX_POINT('',#40209);
#12546=VERTEX_POINT('',#40212);
#12547=VERTEX_POINT('',#40216);
#12548=VERTEX_POINT('',#40219);
#12549=VERTEX_POINT('',#40223);
#12550=VERTEX_POINT('',#40227);
#12551=VERTEX_POINT('',#40230);
#12552=VERTEX_POINT('',#40234);
#12553=VERTEX_POINT('',#40237);
#12554=VERTEX_POINT('',#40241);
#15797=EDGE_CURVE('',#12544,#12545,#10589,.T.);
#15798=EDGE_CURVE('',#12545,#12544,#10590,.T.);
#15799=EDGE_CURVE('',#12544,#12546,#6927,.T.);
#15800=EDGE_CURVE('',#12546,#12546,#10591,.T.);
#15801=EDGE_CURVE('',#12547,#12547,#10592,.T.);
#15802=EDGE_CURVE('',#12548,#12548,#10593,.T.);
#15803=EDGE_CURVE('',#12548,#12545,#6928,.T.);
#15804=EDGE_CURVE('',#12549,#12549,#10594,.T.);
#15805=EDGE_CURVE('',#12549,#12547,#6929,.T.);
#15806=EDGE_CURVE('',#12550,#12550,#10595,.T.);
#15807=EDGE_CURVE('',#12551,#12551,#10596,.T.);
#15808=EDGE_CURVE('',#12551,#12550,#6930,.T.);
#15809=EDGE_CURVE('',#12552,#12552,#10597,.T.);
#15810=EDGE_CURVE('',#12552,#12553,#6931,.T.);
#15811=EDGE_CURVE('',#12553,#12553,#10598,.T.);
#15812=EDGE_CURVE('',#12554,#12554,#10599,.T.);
#15813=EDGE_CURVE('',#12554,#12549,#6932,.T.);
#22088=ORIENTED_EDGE('',*,*,#15797,.T.);
#22089=ORIENTED_EDGE('',*,*,#15798,.T.);
#22090=ORIENTED_EDGE('',*,*,#15799,.T.);
#22091=ORIENTED_EDGE('',*,*,#15800,.T.);
#22092=ORIENTED_EDGE('',*,*,#15799,.F.);
#22093=ORIENTED_EDGE('',*,*,#15800,.F.);
#22094=ORIENTED_EDGE('',*,*,#15801,.T.);
#22095=ORIENTED_EDGE('',*,*,#15802,.F.);
#22096=ORIENTED_EDGE('',*,*,#15803,.T.);
#22097=ORIENTED_EDGE('',*,*,#15797,.F.);
#22098=ORIENTED_EDGE('',*,*,#15798,.F.);
#22099=ORIENTED_EDGE('',*,*,#15803,.F.);
#22100=ORIENTED_EDGE('',*,*,#15804,.T.);
#22101=ORIENTED_EDGE('',*,*,#15805,.T.);
#22102=ORIENTED_EDGE('',*,*,#15801,.F.);
#22103=ORIENTED_EDGE('',*,*,#15805,.F.);
#22104=ORIENTED_EDGE('',*,*,#15806,.F.);
#22105=ORIENTED_EDGE('',*,*,#15802,.T.);
#22106=ORIENTED_EDGE('',*,*,#15807,.F.);
#22107=ORIENTED_EDGE('',*,*,#15808,.T.);
#22108=ORIENTED_EDGE('',*,*,#15806,.T.);
#22109=ORIENTED_EDGE('',*,*,#15808,.F.);
#22110=ORIENTED_EDGE('',*,*,#15807,.T.);
#22111=ORIENTED_EDGE('',*,*,#15809,.F.);
#22112=ORIENTED_EDGE('',*,*,#15809,.T.);
#22113=ORIENTED_EDGE('',*,*,#15810,.T.);
#22114=ORIENTED_EDGE('',*,*,#15811,.F.);
#22115=ORIENTED_EDGE('',*,*,#15810,.F.);
#22116=ORIENTED_EDGE('',*,*,#15811,.T.);
#22117=ORIENTED_EDGE('',*,*,#15812,.F.);
#22118=ORIENTED_EDGE('',*,*,#15812,.T.);
#22119=ORIENTED_EDGE('',*,*,#15813,.T.);
#22120=ORIENTED_EDGE('',*,*,#15804,.F.);
#22121=ORIENTED_EDGE('',*,*,#15813,.F.);
#23590=CONICAL_SURFACE('',#26436,9.47407799863807,1.24294851367413);
#23591=CONICAL_SURFACE('',#26442,10.15,0.915100700553361);
#23592=CONICAL_SURFACE('',#26456,9.07,0.846355413487022);
#24619=ADVANCED_FACE('',(#2760),#23590,.T.);
#24620=ADVANCED_FACE('',(#2761,#657),#1512,.T.);
#24621=ADVANCED_FACE('',(#2762),#23591,.T.);
#24622=ADVANCED_FACE('',(#2763),#523,.F.);
#24623=ADVANCED_FACE('',(#2764,#658),#1513,.T.);
#24624=ADVANCED_FACE('',(#2765),#524,.T.);
#24625=ADVANCED_FACE('',(#2766,#659),#1514,.T.);
#24626=ADVANCED_FACE('',(#2767),#525,.F.);
#24627=ADVANCED_FACE('',(#2768,#660),#1515,.T.);
#24628=ADVANCED_FACE('',(#2769),#23592,.F.);
#24943=CLOSED_SHELL('',(#24619,#24620,#24621,#24622,#24623,#24624,#24625,
#24626,#24627,#24628));
#26435=AXIS2_PLACEMENT_3D('',#40206,#31984,#31985);
#26436=AXIS2_PLACEMENT_3D('',#40207,#31986,#31987);
#26437=AXIS2_PLACEMENT_3D('',#40210,#31988,#31989);
#26438=AXIS2_PLACEMENT_3D('',#40211,#31990,#31991);
#26439=AXIS2_PLACEMENT_3D('',#40214,#31993,#31994);
#26440=AXIS2_PLACEMENT_3D('',#40215,#31995,#31996);
#26441=AXIS2_PLACEMENT_3D('',#40217,#31997,#31998);
#26442=AXIS2_PLACEMENT_3D('',#40218,#31999,#32000);
#26443=AXIS2_PLACEMENT_3D('',#40220,#32001,#32002);
#26444=AXIS2_PLACEMENT_3D('',#40222,#32004,#32005);
#26445=AXIS2_PLACEMENT_3D('',#40224,#32006,#32007);
#26446=AXIS2_PLACEMENT_3D('',#40226,#32009,#32010);
#26447=AXIS2_PLACEMENT_3D('',#40228,#32011,#32012);
#26448=AXIS2_PLACEMENT_3D('',#40229,#32013,#32014);
#26449=AXIS2_PLACEMENT_3D('',#40231,#32015,#32016);
#26450=AXIS2_PLACEMENT_3D('',#40233,#32018,#32019);
#26451=AXIS2_PLACEMENT_3D('',#40235,#32020,#32021);
#26452=AXIS2_PLACEMENT_3D('',#40236,#32022,#32023);
#26453=AXIS2_PLACEMENT_3D('',#40239,#32025,#32026);
#26454=AXIS2_PLACEMENT_3D('',#40240,#32027,#32028);
#26455=AXIS2_PLACEMENT_3D('',#40242,#32029,#32030);
#26456=AXIS2_PLACEMENT_3D('',#40243,#32031,#32032);
#31984=DIRECTION('axis',(0.,0.,1.));
#31985=DIRECTION('refdir',(1.,0.,0.));
#31986=DIRECTION('center_axis',(1.,0.,-3.89588521716247E-15));
#31987=DIRECTION('ref_axis',(0.,-1.,-3.13402942782487E-17));
#31988=DIRECTION('center_axis',(-1.,0.,0.));
#31989=DIRECTION('ref_axis',(0.,-1.,-6.12323399573677E-17));
#31990=DIRECTION('center_axis',(-1.,0.,0.));
#31991=DIRECTION('ref_axis',(0.,-1.,-6.12323399573677E-17));
#31992=DIRECTION('',(-0.322006219579217,-0.946737553154147,1.10888632576264E-15));
#31993=DIRECTION('center_axis',(1.,0.,0.));
#31994=DIRECTION('ref_axis',(0.,-1.,0.));
#31995=DIRECTION('center_axis',(-1.,0.,0.));
#31996=DIRECTION('ref_axis',(0.,0.,1.));
#31997=DIRECTION('center_axis',(1.,0.,0.));
#31998=DIRECTION('ref_axis',(0.,0.,-1.));
#31999=DIRECTION('center_axis',(1.,0.,0.));
#32000=DIRECTION('ref_axis',(0.,1.,0.));
#32001=DIRECTION('center_axis',(1.,0.,0.));
#32002=DIRECTION('ref_axis',(0.,0.,-1.));
#32003=DIRECTION('',(-0.609710760849692,0.7926239891046,9.70684431184355E-17));
#32004=DIRECTION('center_axis',(1.,0.,0.));
#32005=DIRECTION('ref_axis',(0.,1.,0.));
#32006=DIRECTION('center_axis',(1.,0.,0.));
#32007=DIRECTION('ref_axis',(0.,0.,-1.));
#32008=DIRECTION('',(-1.,0.,0.));
#32009=DIRECTION('center_axis',(-1.,0.,0.));
#32010=DIRECTION('ref_axis',(0.,0.,1.));
#32011=DIRECTION('center_axis',(1.,0.,0.));
#32012=DIRECTION('ref_axis',(0.,0.,-1.));
#32013=DIRECTION('center_axis',(1.,0.,0.));
#32014=DIRECTION('ref_axis',(0.,1.,0.));
#32015=DIRECTION('center_axis',(1.,0.,0.));
#32016=DIRECTION('ref_axis',(0.,0.,-1.));
#32017=DIRECTION('',(-1.,0.,0.));
#32018=DIRECTION('center_axis',(1.,0.,0.));
#32019=DIRECTION('ref_axis',(0.,0.,-1.));
#32020=DIRECTION('center_axis',(1.,0.,0.));
#32021=DIRECTION('ref_axis',(0.,0.,-1.));
#32022=DIRECTION('center_axis',(1.,0.,0.));
#32023=DIRECTION('ref_axis',(0.,1.,0.));
#32024=DIRECTION('',(-1.,0.,0.));
#32025=DIRECTION('center_axis',(1.,0.,0.));
#32026=DIRECTION('ref_axis',(0.,0.,-1.));
#32027=DIRECTION('center_axis',(1.,0.,0.));
#32028=DIRECTION('ref_axis',(0.,0.,-1.));
#32029=DIRECTION('center_axis',(1.,0.,0.));
#32030=DIRECTION('ref_axis',(0.,0.,-1.));
#32031=DIRECTION('center_axis',(1.,0.,0.));
#32032=DIRECTION('ref_axis',(0.,1.,0.));
#32033=DIRECTION('',(-0.662716862978517,0.748870055165724,9.17101316036005E-17));
#40206=CARTESIAN_POINT('',(0.,0.,0.));
#40207=CARTESIAN_POINT('Origin',(0.0762138451062111,0.,-2.96920392492399E-16));
#40208=CARTESIAN_POINT('',(0.152427690212422,9.69815599727615,-1.18768156996959E-15));
#40209=CARTESIAN_POINT('',(0.152427690212421,-9.69815599727615,-1.18768156996959E-15));
#40210=CARTESIAN_POINT('Origin',(0.152427690212422,0.,-5.93840784984797E-16));
#40211=CARTESIAN_POINT('Origin',(0.152427690212422,0.,-5.93840784984797E-16));
#40212=CARTESIAN_POINT('',(0.,9.25,1.1327982892113E-15));
#40213=CARTESIAN_POINT('',(0.0762138451062111,9.47407799863807,1.16023992959045E-15));
#40214=CARTESIAN_POINT('Origin',(0.,0.,0.));
#40215=CARTESIAN_POINT('Origin',(0.,9.5,0.));
#40216=CARTESIAN_POINT('',(0.,-7.94,-9.72369558522999E-16));
#40217=CARTESIAN_POINT('Origin',(0.,0.,0.));
#40218=CARTESIAN_POINT('Origin',(0.5,0.,0.));
#40219=CARTESIAN_POINT('',(1.,-10.8,-1.32261854307914E-15));
#40220=CARTESIAN_POINT('Origin',(1.,0.,0.));
#40221=CARTESIAN_POINT('',(0.5,-10.15,-1.24301650113456E-15));
#40222=CARTESIAN_POINT('Origin',(1.5,0.,0.));
#40223=CARTESIAN_POINT('',(3.,-7.94,-9.72369558522999E-16));
#40224=CARTESIAN_POINT('Origin',(3.,0.,0.));
#40225=CARTESIAN_POINT('',(1.5,-7.94,-9.72369558522999E-16));
#40226=CARTESIAN_POINT('Origin',(1.,14.29,0.));
#40227=CARTESIAN_POINT('',(1.,-14.29,-1.75002027598157E-15));
#40228=CARTESIAN_POINT('Origin',(1.,0.,0.));
#40229=CARTESIAN_POINT('Origin',(3.675,0.,0.));
#40230=CARTESIAN_POINT('',(6.35,-14.29,-1.75002027598157E-15));
#40231=CARTESIAN_POINT('Origin',(6.35,0.,0.));
#40232=CARTESIAN_POINT('',(3.675,-14.29,-1.75002027598157E-15));
#40233=CARTESIAN_POINT('Origin',(6.35,12.,0.));
#40234=CARTESIAN_POINT('',(6.35,-12.,-1.46957615897682E-15));
#40235=CARTESIAN_POINT('Origin',(6.35,0.,0.));
#40236=CARTESIAN_POINT('Origin',(5.675,0.,0.));
#40237=CARTESIAN_POINT('',(5.,-12.,-1.46957615897682E-15));
#40238=CARTESIAN_POINT('',(5.675,-12.,-1.46957615897682E-15));
#40239=CARTESIAN_POINT('Origin',(5.,0.,0.));
#40240=CARTESIAN_POINT('Origin',(5.,10.2,0.));
#40241=CARTESIAN_POINT('',(5.,-10.2,-1.2491397351303E-15));
#40242=CARTESIAN_POINT('Origin',(5.,0.,0.));
#40243=CARTESIAN_POINT('Origin',(4.,0.,0.));
#40244=CARTESIAN_POINT('',(4.,-9.07,-1.11075464682665E-15));
#46371=UNCERTAINTY_MEASURE_WITH_UNIT(LENGTH_MEASURE(0.01),#46396,
'DISTANCE_ACCURACY_VALUE',
'Maximum model space distance between geometric entities at asserted c
onnectivities');
#46379=UNCERTAINTY_MEASURE_WITH_UNIT(LENGTH_MEASURE(0.01),#46396,
'DISTANCE_ACCURACY_VALUE',
'Maximum model space distance between geometric entities at asserted c
onnectivities');
#46387=(
GEOMETRIC_REPRESENTATION_CONTEXT(3)
GLOBAL_UNCERTAINTY_ASSIGNED_CONTEXT((#46371))
GLOBAL_UNIT_ASSIGNED_CONTEXT((#46396,#46398,#46399))
REPRESENTATION_CONTEXT('','3D')
);
#46395=(
GEOMETRIC_REPRESENTATION_CONTEXT(3)
GLOBAL_UNCERTAINTY_ASSIGNED_CONTEXT((#46379))
GLOBAL_UNIT_ASSIGNED_CONTEXT((#46396,#46398,#46399))
REPRESENTATION_CONTEXT('','3D')
);
#46396=(
LENGTH_UNIT()
NAMED_UNIT(*)
SI_UNIT(.MILLI.,.METRE.)
);
#46398=(
NAMED_UNIT(*)
PLANE_ANGLE_UNIT()
SI_UNIT($,.RADIAN.)
);
#46399=(
NAMED_UNIT(*)
SI_UNIT($,.STERADIAN.)
SOLID_ANGLE_UNIT()
);
#46407=SHAPE_DEFINITION_REPRESENTATION(#46422,#46462);
#46422=PRODUCT_DEFINITION_SHAPE('',$,#46478);
#46462=SHAPE_REPRESENTATION('',(#26435),#46387);
#46470=PRODUCT_DEFINITION_CONTEXT('part definition',#46517,'design');
#46478=PRODUCT_DEFINITION('2026-10-26-00-51-13-026',
'08_Shaft_Lip_Seal_5-8x1-1-8',#46493,#46470);
#46493=PRODUCT_DEFINITION_FORMATION('',$,#46526);
#46517=APPLICATION_CONTEXT(
'Core Data for Automotive Mechanical Design Process');
#46518=PRODUCT_CONTEXT('part definition',#46517,'mechanical');
#46526=PRODUCT('2026-10-26-00-51-13-026','08_Shaft_Lip_Seal_5-8x1-1-8',
$,(#46518));
#46597=COLOUR_RGB('Black',0.12,0.14,0.17);
#46598=FILL_AREA_STYLE_COLOUR('',#46597);
#46599=FILL_AREA_STYLE('',(#46598));
#46600=SURFACE_STYLE_FILL_AREA(#46599);
#46601=SURFACE_SIDE_STYLE('',(#46600));
#46602=SURFACE_STYLE_USAGE(.BOTH.,#46601);
#46603=PRESENTATION_STYLE_ASSIGNMENT((#46602));
ENDSEC;
END-ISO-10303-21;
